ISO-10303-21;
HEADER;
FILE_DESCRIPTION (('STEP AP214'),
    '1' );
FILE_NAME ('MirrorSlot.step',
    '2026-10-21T17:07:05',
    ( '' ),
    ( '' ),
    'SwSTEP 2.0',
    'SolidWorks 2025',
    '' );
FILE_SCHEMA (( 'AUTOMOTIVE_DESIGN' ));
ENDSEC;

DATA;
#372=CARTESIAN_POINT ( 'NONE',  ( 799.9999999999993179, -365.3551492539851893, 18.13243251470705886 ) ) ;
#531=AXIS2_PLACEMENT_3D ( 'NONE', #37284, #44217, #1707 ) ;
#606=DIRECTION ( 'NONE',  ( -1.000000000000000000, -0.000000000000000000, 0.000000000000000000 ) ) ;
#665=EDGE_CURVE ( 'NONE', #10985, #9763, #35048, .T. ) ;
#712=LINE ( 'NONE', #43645, #30692 ) ;
#769=CARTESIAN_POINT ( 'NONE',  ( 799.9999999999993179, -365.3551492539851893, 28.13243251470704109 ) ) ;
#1125=DIRECTION ( 'NONE',  ( 0.000000000000000000, 0.000000000000000000, -1.000000000000000000 ) ) ;
#1210=ORIENTED_EDGE ( 'NONE', *, *, #20424, .F. ) ;
#1693=ORIENTED_EDGE ( 'NONE', *, *, #19596, .T. ) ;
#1707=DIRECTION ( 'NONE',  ( 0.000000000000000000, 0.000000000000000000, 1.000000000000000000 ) ) ;
#1825=ORIENTED_EDGE ( 'NONE', *, *, #4000, .F. ) ;
#1937=MANIFOLD_SOLID_BREP ( '<Slot>-<Boss-Extrude21>', #29843 ) ;
#1950=LINE ( 'NONE', #5881, #31862 ) ;
#2023=AXIS2_PLACEMENT_3D ( 'NONE', #40515, #8866, #22932 ) ;
#2395=EDGE_CURVE ( 'NONE', #10343, #38198, #15093, .T. ) ;
#2482=FACE_OUTER_BOUND ( 'NONE', #43857, .T. ) ;
#2486=DIRECTION ( 'NONE',  ( 0.000000000000000000, 0.000000000000000000, 1.000000000000000000 ) ) ;
#2631=PRODUCT ( 'MirrorSlot', 'MirrorSlot', '', ( #40907 ) ) ;
#2770=CARTESIAN_POINT ( 'NONE',  ( 794.9999999999993179, 205.0000000000000568, 265.0000000000000000 ) ) ;
#2928=CARTESIAN_POINT ( 'NONE',  ( 794.9999999999993179, -357.6843811873878280, -0.3380660510726891665 ) ) ;
#3257=CARTESIAN_POINT ( 'NONE',  ( 794.9999999999993179, 205.0000000000000568, 245.0000000000000284 ) ) ;
#3275=AXIS2_PLACEMENT_3D ( 'NONE', #9976, #20811, #24047 ) ;
#3406=LINE ( 'NONE', #41291, #31582 ) ;
#3419=ORIENTED_EDGE ( 'NONE', *, *, #32569, .F. ) ;
#3530=AXIS2_PLACEMENT_3D ( 'NONE', #4233, #14156, #36304 ) ;
#3737=FACE_OUTER_BOUND ( 'NONE', #34936, .T. ) ;
#3789=EDGE_CURVE ( 'NONE', #44896, #39863, #40665, .T. ) ;
#3931=ORIENTED_EDGE ( 'NONE', *, *, #3789, .F. ) ;
#3984=FACE_OUTER_BOUND ( 'NONE', #23947, .T. ) ;
#4000=EDGE_CURVE ( 'NONE', #36366, #39863, #29876, .T. ) ;
#4134=DIRECTION ( 'NONE',  ( 0.000000000000000000, 0.000000000000000000, 1.000000000000000000 ) ) ;
#4233=CARTESIAN_POINT ( 'NONE',  ( 799.9999999999993179, 205.0000000000000568, 255.0000000000000000 ) ) ;
#4453=CYLINDRICAL_SURFACE ( 'NONE', #27857, 9.999999999999980460 ) ;
#4668=( NAMED_UNIT ( * ) SI_UNIT ( $, .STERADIAN. ) SOLID_ANGLE_UNIT ( ) );
#4743=FACE_OUTER_BOUND ( 'NONE', #11728, .T. ) ;
#4853=DIRECTION ( 'NONE',  ( -1.000000000000000000, -0.000000000000000000, 0.000000000000000000 ) ) ;
#5059=VERTEX_POINT ( 'NONE', #11629 ) ;
#5064=CARTESIAN_POINT ( 'NONE',  ( 799.9999999999993179, 205.0000000000000568, 265.0000000000000000 ) ) ;
#5181=DIRECTION ( 'NONE',  ( -1.000000000000000000, -0.000000000000000000, -0.000000000000000000 ) ) ;
#5233=EDGE_CURVE ( 'NONE', #42700, #9048, #40360, .T. ) ;
#5264=CARTESIAN_POINT ( 'NONE',  ( 799.9999999999993179, 197.3292319334027241, 273.4704985657796783 ) ) ;
#5584=CARTESIAN_POINT ( 'NONE',  ( 799.9999999999993179, 205.0000000000000568, 255.0000000000000000 ) ) ;
#5643=CIRCLE ( 'NONE', #9346, 19.99999999999990763 ) ;
#5806=SHAPE_DEFINITION_REPRESENTATION ( #16262, #28884 ) ;
#5846=FACE_BOUND ( 'NONE', #7949, .T. ) ;
#5881=CARTESIAN_POINT ( 'NONE',  ( 794.9999999999993179, 212.6707680665973612, 236.5295014342203785 ) ) ;
#5941=ORIENTED_EDGE ( 'NONE', *, *, #24651, .T. ) ;
#6075=DIRECTION ( 'NONE',  ( 1.000000000000000000, 0.000000000000000000, 0.000000000000000000 ) ) ;
#6324=CARTESIAN_POINT ( 'NONE',  ( 794.9999999999993179, 197.3292319334027241, 273.4704985657796783 ) ) ;
#6472=CARTESIAN_POINT ( 'NONE',  ( 799.9999999999993179, -365.3551492539851893, 8.132432514707076621 ) ) ;
#6913=CIRCLE ( 'NONE', #29050, 9.999999999999980460 ) ;
#6986=AXIS2_PLACEMENT_3D ( 'NONE', #40613, #37368, #12652 ) ;
#7101=AXIS2_PLACEMENT_3D ( 'NONE', #27862, #41957, #10299 ) ;
#7608=( GEOMETRIC_REPRESENTATION_CONTEXT ( 3 ) GLOBAL_UNCERTAINTY_ASSIGNED_CONTEXT ( ( #45520 ) ) GLOBAL_UNIT_ASSIGNED_CONTEXT ( ( #36091, #25692, #4668 ) ) REPRESENTATION_CONTEXT ( 'NONE', 'WORKASPACE' ) );
#7690=ORIENTED_EDGE ( 'NONE', *, *, #32569, .T. ) ;
#7712=ADVANCED_FACE ( 'NONE', ( #3737 ), #18738, .T. ) ;
#7781=AXIS2_PLACEMENT_3D ( 'NONE', #14828, #21505, #36064 ) ;
#7949=EDGE_LOOP ( 'NONE', ( #42912, #32586 ) ) ;
#8199=ORIENTED_EDGE ( 'NONE', *, *, #38844, .T. ) ;
#8406=CARTESIAN_POINT ( 'NONE',  ( 794.9999999999993179, 205.0000000000000568, 255.0000000000000000 ) ) ;
#8696=CARTESIAN_POINT ( 'NONE',  ( 799.9999999999993179, 205.0000000000000568, 245.0000000000000284 ) ) ;
#8866=DIRECTION ( 'NONE',  ( -1.000000000000000000, -0.000000000000000000, -0.000000000000000000 ) ) ;
#9048=VERTEX_POINT ( 'NONE', #42171 ) ;
#9214=EDGE_CURVE ( 'NONE', #38198, #16659, #39181, .T. ) ;
#9312=FACE_BOUND ( 'NONE', #36246, .T. ) ;
#9346=AXIS2_PLACEMENT_3D ( 'NONE', #40690, #33532, #25915 ) ;
#9748=EDGE_CURVE ( 'NONE', #9048, #42700, #35118, .T. ) ;
#9763=VERTEX_POINT ( 'NONE', #26204 ) ;
#9863=CARTESIAN_POINT ( 'NONE',  ( 794.9999999999993179, -365.3551492539851893, 18.13243251470705886 ) ) ;
#9899=ORIENTED_EDGE ( 'NONE', *, *, #22960, .F. ) ;
#9976=CARTESIAN_POINT ( 'NONE',  ( 799.9999999999993179, -365.3551492539851893, 18.13243251470705886 ) ) ;
#10022=DIRECTION ( 'NONE',  ( 0.000000000000000000, 0.9235249282889856914, 0.3835384033298670503 ) ) ;
#10081=PLANE ( 'NONE',  #12230 ) ;
#10299=DIRECTION ( 'NONE',  ( 0.000000000000000000, 0.000000000000000000, 1.000000000000000000 ) ) ;
#10343=VERTEX_POINT ( 'NONE', #769 ) ;
#10433=APPLICATION_CONTEXT ( 'automotive_design' ) ;
#10628=DIRECTION ( 'NONE',  ( -1.000000000000000000, -0.000000000000000000, 0.000000000000000000 ) ) ;
#10644=AXIS2_PLACEMENT_3D ( 'NONE', #21127, #28512, #21351 ) ;
#10732=EDGE_CURVE ( 'NONE', #29534, #44896, #5643, .T. ) ;
#10985=VERTEX_POINT ( 'NONE', #44616 ) ;
#11000=DIRECTION ( 'NONE',  ( -1.000000000000000000, -0.000000000000000000, 0.000000000000000000 ) ) ;
#11076=CARTESIAN_POINT ( 'NONE',  ( 799.9999999999993179, 205.0000000000000568, 255.0000000000000000 ) ) ;
#11457=CARTESIAN_POINT ( 'NONE',  ( 799.9999999999993179, 212.6707680665973612, 236.5295014342203785 ) ) ;
#11522=LINE ( 'NONE', #36677, #29682 ) ;
#11629=CARTESIAN_POINT ( 'NONE',  ( 794.9999999999993179, -373.0259173205825505, 36.60293108048681887 ) ) ;
#11649=CARTESIAN_POINT ( 'NONE',  ( 799.9999999999993179, -365.3551492539851893, 18.13243251470705886 ) ) ;
#11700=CARTESIAN_POINT ( 'NONE',  ( 799.9999999999993179, 212.6707680665973612, 236.5295014342203785 ) ) ;
#11728=EDGE_LOOP ( 'NONE', ( #37258, #29566, #5941, #33822 ) ) ;
#11767=DIRECTION ( 'NONE',  ( -1.000000000000000000, -0.000000000000000000, 0.000000000000000000 ) ) ;
#11781=ORIENTED_EDGE ( 'NONE', *, *, #2395, .T. ) ;
#11864=DIRECTION ( 'NONE',  ( 0.000000000000000000, 0.000000000000000000, -1.000000000000000000 ) ) ;
#11999=ORIENTED_EDGE ( 'NONE', *, *, #2395, .F. ) ;
#12092=FACE_OUTER_BOUND ( 'NONE', #20619, .T. ) ;
#12134=DIRECTION ( 'NONE',  ( 0.000000000000000000, -0.9235249282889854694, -0.3835384033298675499 ) ) ;
#12219=VERTEX_POINT ( 'NONE', #2928 ) ;
#12230=AXIS2_PLACEMENT_3D ( 'NONE', #24153, #38262, #20684 ) ;
#12312=DIRECTION ( 'NONE',  ( -1.000000000000000000, -0.000000000000000000, -0.000000000000000000 ) ) ;
#12519=CARTESIAN_POINT ( 'NONE',  ( 794.9999999999993179, 212.6707680665973612, 236.5295014342203785 ) ) ;
#12587=EDGE_CURVE ( 'NONE', #44896, #31811, #18848, .T. ) ;
#12652=DIRECTION ( 'NONE',  ( 0.000000000000000000, 0.000000000000000000, 1.000000000000000000 ) ) ;
#12854=VECTOR ( 'NONE', #15829, 1000.000000000000000 ) ;
#13488=CARTESIAN_POINT ( 'NONE',  ( 794.9999999999993179, -365.3551492539851893, 18.13243251470705886 ) ) ;
#14138=DIRECTION ( 'NONE',  ( 0.000000000000000000, 0.000000000000000000, 1.000000000000000000 ) ) ;
#14156=DIRECTION ( 'NONE',  ( -1.000000000000000000, -0.000000000000000000, 0.000000000000000000 ) ) ;
#14431=PLANE ( 'NONE',  #10644 ) ;
#14518=ORIENTED_EDGE ( 'NONE', *, *, #28880, .F. ) ;
#14556=FACE_OUTER_BOUND ( 'NONE', #24700, .T. ) ;
#14702=ORIENTED_EDGE ( 'NONE', *, *, #10732, .F. ) ;
#14782=LINE ( 'NONE', #42935, #38677 ) ;
#14828=CARTESIAN_POINT ( 'NONE',  ( 799.9999999999993179, -365.3551492539851893, 18.13243251470705886 ) ) ;
#15093=CIRCLE ( 'NONE', #3275, 9.999999999999980460 ) ;
#15185=APPLICATION_CONTEXT ( 'automotive_design' ) ;
#15311=CIRCLE ( 'NONE', #531, 20.00000000000004619 ) ;
#15344=DIRECTION ( 'NONE',  ( -1.000000000000000000, -0.000000000000000000, 0.000000000000000000 ) ) ;
#15366=ORIENTED_EDGE ( 'NONE', *, *, #27158, .F. ) ;
#15383=DIRECTION ( 'NONE',  ( 0.000000000000000000, -0.9235249282889854694, -0.3835384033298675499 ) ) ;
#15463=ORIENTED_EDGE ( 'NONE', *, *, #5233, .T. ) ;
#15545=CARTESIAN_POINT ( 'NONE',  ( 794.9999999999993179, -365.3551492539851893, 18.13243251470705886 ) ) ;
#15829=DIRECTION ( 'NONE',  ( -1.000000000000000000, -0.000000000000000000, 0.000000000000000000 ) ) ;
#15927=CYLINDRICAL_SURFACE ( 'NONE', #41779, 9.999999999999982236 ) ;
#15993=EDGE_CURVE ( 'NONE', #39863, #12219, #1950, .T. ) ;
#15994=DIRECTION ( 'NONE',  ( -1.000000000000000000, -0.000000000000000000, -0.000000000000000000 ) ) ;
#16262=PRODUCT_DEFINITION_SHAPE ( 'NONE', 'NONE',  #22809 ) ;
#16461=CARTESIAN_POINT ( 'NONE',  ( 799.9999999999993179, -357.6843811873878280, -0.3380660510726891665 ) ) ;
#16659=VERTEX_POINT ( 'NONE', #24797 ) ;
#16681=CIRCLE ( 'NONE', #21858, 10.00000000000000888 ) ;
#16772=ORIENTED_EDGE ( 'NONE', *, *, #29199, .T. ) ;
#16929=LINE ( 'NONE', #16461, #23977 ) ;
#17418=ORIENTED_EDGE ( 'NONE', *, *, #36127, .T. ) ;
#17654=ORIENTED_EDGE ( 'NONE', *, *, #34495, .T. ) ;
#18075=AXIS2_PLACEMENT_3D ( 'NONE', #11649, #15344, #11864 ) ;
#18238=ORIENTED_EDGE ( 'NONE', *, *, #34495, .F. ) ;
#18319=VERTEX_POINT ( 'NONE', #2770 ) ;
#18361=FACE_OUTER_BOUND ( 'NONE', #42921, .T. ) ;
#18542=CARTESIAN_POINT ( 'NONE',  ( 799.9999999999993179, 205.0000000000000568, 255.0000000000000000 ) ) ;
#18689=DIRECTION ( 'NONE',  ( -1.000000000000000000, -0.000000000000000000, 0.000000000000000000 ) ) ;
#18738=CYLINDRICAL_SURFACE ( 'NONE', #7781, 20.00000000000004974 ) ;
#18848=LINE ( 'NONE', #11457, #45464 ) ;
#18855=AXIS2_PLACEMENT_3D ( 'NONE', #22121, #29303, #4134 ) ;
#19156=DIRECTION ( 'NONE',  ( -1.000000000000000000, -0.000000000000000000, 0.000000000000000000 ) ) ;
#19454=( NAMED_UNIT ( * ) SI_UNIT ( $, .STERADIAN. ) SOLID_ANGLE_UNIT ( ) );
#19484=ORIENTED_EDGE ( 'NONE', *, *, #15993, .T. ) ;
#19555=VECTOR ( 'NONE', #26789, 1000.000000000000000 ) ;
#19596=EDGE_CURVE ( 'NONE', #16659, #22935, #24017, .T. ) ;
#19816=FACE_BOUND ( 'NONE', #32471, .T. ) ;
#19932=CARTESIAN_POINT ( 'NONE',  ( 794.9999999999993179, -365.3551492539851893, 28.13243251470704109 ) ) ;
#20066=CARTESIAN_POINT ( 'NONE',  ( 794.9999999999993179, -365.3551492539851893, -1.867567485292990437 ) ) ;
#20415=AXIS2_PLACEMENT_3D ( 'NONE', #5584, #15994, #23801 ) ;
#20424=EDGE_CURVE ( 'NONE', #9048, #40061, #32718, .T. ) ;
#20560=EDGE_LOOP ( 'NONE', ( #38877, #39328, #40917, #1210 ) ) ;
#20619=EDGE_LOOP ( 'NONE', ( #11999, #41427, #24368, #43464 ) ) ;
#20684=DIRECTION ( 'NONE',  ( 0.000000000000000000, -0.9235249282889858025, -0.3835384033298669948 ) ) ;
#20811=DIRECTION ( 'NONE',  ( -1.000000000000000000, -0.000000000000000000, -0.000000000000000000 ) ) ;
#21031=ADVANCED_FACE ( 'NONE', ( #18361 ), #14431, .F. ) ;
#21127=CARTESIAN_POINT ( 'NONE',  ( 799.9999999999993179, 212.6707680665973612, 236.5295014342203785 ) ) ;
#21351=DIRECTION ( 'NONE',  ( 0.000000000000000000, 0.9235249282889854694, 0.3835384033298675499 ) ) ;
#21418=ADVANCED_FACE ( 'NONE', ( #12092 ), #25498, .F. ) ;
#21505=DIRECTION ( 'NONE',  ( -1.000000000000000000, -0.000000000000000000, 0.000000000000000000 ) ) ;
#21823=CIRCLE ( 'NONE', #7101, 9.999999999999980460 ) ;
#21858=AXIS2_PLACEMENT_3D ( 'NONE', #36916, #30677, #2486 ) ;
#22019=VECTOR ( 'NONE', #10628, 1000.000000000000000 ) ;
#22050=ORIENTED_EDGE ( 'NONE', *, *, #24651, .F. ) ;
#22121=CARTESIAN_POINT ( 'NONE',  ( 794.9999999999993179, 205.0000000000000568, 255.0000000000000000 ) ) ;
#22605=LINE ( 'NONE', #5064, #40876 ) ;
#22706=FACE_OUTER_BOUND ( 'NONE', #43566, .T. ) ;
#22809=PRODUCT_DEFINITION ( 'UNKNOWN', '', #31953, #43961 ) ;
#22825=VECTOR ( 'NONE', #10022, 1000.000000000000114 ) ;
#22910=ADVANCED_FACE ( 'NONE', ( #22706, #9312, #5846 ), #32901, .F. ) ;
#22932=DIRECTION ( 'NONE',  ( 0.000000000000000000, 0.000000000000000000, 1.000000000000000000 ) ) ;
#22935=VERTEX_POINT ( 'NONE', #19932 ) ;
#22960=EDGE_CURVE ( 'NONE', #31811, #12219, #16929, .T. ) ;
#22983=ORIENTED_EDGE ( 'NONE', *, *, #22960, .T. ) ;
#23015=CARTESIAN_POINT ( 'NONE',  ( 794.9999999999993179, 205.0000000000000568, 255.0000000000000000 ) ) ;
#23153=CARTESIAN_POINT ( 'NONE',  ( 0.000000000000000000, 0.000000000000000000, 0.000000000000000000 ) ) ;
#23166=DIRECTION ( 'NONE',  ( 0.000000000000000000, 0.000000000000000000, 1.000000000000000000 ) ) ;
#23326=ADVANCED_FACE ( 'NONE', ( #41727 ), #10081, .F. ) ;
#23454=EDGE_CURVE ( 'NONE', #38198, #10343, #21823, .T. ) ;
#23801=DIRECTION ( 'NONE',  ( 0.000000000000000000, 0.000000000000000000, 1.000000000000000000 ) ) ;
#23935=DIRECTION ( 'NONE',  ( -1.000000000000000000, -0.000000000000000000, -0.000000000000000000 ) ) ;
#23947=EDGE_LOOP ( 'NONE', ( #14518, #37960, #42200, #7690 ) ) ;
#23977=VECTOR ( 'NONE', #38180, 1000.000000000000000 ) ;
#24017=CIRCLE ( 'NONE', #41754, 9.999999999999980460 ) ;
#24047=DIRECTION ( 'NONE',  ( 0.000000000000000000, 0.000000000000000000, 1.000000000000000000 ) ) ;
#24153=CARTESIAN_POINT ( 'NONE',  ( 799.9999999999993179, 197.3292319334027241, 273.4704985657796783 ) ) ;
#24248=UNCERTAINTY_MEASURE_WITH_UNIT (LENGTH_MEASURE( 1.000000000000000082E-05 ), #37231, 'distance_accuracy_value', 'NONE');
#24368=ORIENTED_EDGE ( 'NONE', *, *, #28336, .T. ) ;
#24387=CARTESIAN_POINT ( 'NONE',  ( 799.9999999999993179, 205.0000000000000568, 265.0000000000000000 ) ) ;
#24490=ORIENTED_EDGE ( 'NONE', *, *, #38844, .F. ) ;
#24651=EDGE_CURVE ( 'NONE', #9763, #5059, #712, .T. ) ;
#24691=ADVANCED_FACE ( 'NONE', ( #40427 ), #15927, .F. ) ;
#24700=EDGE_LOOP ( 'NONE', ( #1825, #40416, #26073, #42437 ) ) ;
#24797=CARTESIAN_POINT ( 'NONE',  ( 794.9999999999993179, -365.3551492539851893, 8.132432514707076621 ) ) ;
#25498=CYLINDRICAL_SURFACE ( 'NONE', #18075, 9.999999999999982236 ) ;
#25692=( NAMED_UNIT ( * ) PLANE_ANGLE_UNIT ( ) SI_UNIT ( $, .RADIAN. ) );
#25915=DIRECTION ( 'NONE',  ( 0.000000000000000000, 0.000000000000000000, 1.000000000000000000 ) ) ;
#26073=ORIENTED_EDGE ( 'NONE', *, *, #10732, .T. ) ;
#26155=DIRECTION ( 'NONE',  ( 0.000000000000000000, 0.000000000000000000, 1.000000000000000000 ) ) ;
#26204=CARTESIAN_POINT ( 'NONE',  ( 799.9999999999993179, -373.0259173205825505, 36.60293108048681887 ) ) ;
#26467=ORIENTED_EDGE ( 'NONE', *, *, #15993, .F. ) ;
#26521=AXIS2_PLACEMENT_3D ( 'NONE', #13488, #45362, #28020 ) ;
#26789=DIRECTION ( 'NONE',  ( -1.000000000000000000, -0.000000000000000000, 0.000000000000000000 ) ) ;
#26858=AXIS2_PLACEMENT_3D ( 'NONE', #23153, #34241, #6075 ) ;
#26918=ADVANCED_FACE ( 'NONE', ( #4743 ), #32001, .T. ) ;
#27005=CARTESIAN_POINT ( 'NONE',  ( 799.9999999999993179, -365.3551492539851893, 18.13243251470705886 ) ) ;
#27094=CIRCLE ( 'NONE', #2023, 20.00000000000004619 ) ;
#27096=CARTESIAN_POINT ( 'NONE',  ( 799.9999999999993179, -357.6843811873878280, -0.3380660510726891665 ) ) ;
#27158=EDGE_CURVE ( 'NONE', #12219, #40969, #15311, .T. ) ;
#27200=ORIENTED_EDGE ( 'NONE', *, *, #41642, .F. ) ;
#27467=AXIS2_PLACEMENT_3D ( 'NONE', #23015, #43156, #40598 ) ;
#27526=DIRECTION ( 'NONE',  ( -1.000000000000000000, -0.000000000000000000, -0.000000000000000000 ) ) ;
#27738=AXIS2_PLACEMENT_3D ( 'NONE', #37042, #5181, #23166 ) ;
#27857=AXIS2_PLACEMENT_3D ( 'NONE', #18542, #32621, #40463 ) ;
#27862=CARTESIAN_POINT ( 'NONE',  ( 799.9999999999993179, -365.3551492539851893, 18.13243251470705886 ) ) ;
#28020=DIRECTION ( 'NONE',  ( 0.000000000000000000, 0.000000000000000000, 1.000000000000000000 ) ) ;
#28176=CARTESIAN_POINT ( 'NONE',  ( 799.9999999999993179, 197.3292319334027241, 273.4704985657796783 ) ) ;
#28336=EDGE_CURVE ( 'NONE', #22935, #16659, #6913, .T. ) ;
#28356=STYLED_ITEM('',(#45751),#1937);
#28390=AXIS2_PLACEMENT_3D ( 'NONE', #45100, #27526, #14138 ) ;
#28512=DIRECTION ( 'NONE',  ( 0.000000000000000000, -0.3835384033298676054, 0.9235249282889855804 ) ) ;
#28659=ORIENTED_EDGE ( 'NONE', *, *, #27158, .T. ) ;
#28768=ORIENTED_EDGE ( 'NONE', *, *, #36127, .F. ) ;
#28880=EDGE_CURVE ( 'NONE', #42700, #18319, #22605, .T. ) ;
#28884=SHAPE_REPRESENTATION ( 'MirrorSlot', ( #26858 ), #7608 ) ;
#29050=AXIS2_PLACEMENT_3D ( 'NONE', #15545, #12312, #26155 ) ;
#29199=EDGE_CURVE ( 'NONE', #10985, #40969, #14782, .T. ) ;
#29303=DIRECTION ( 'NONE',  ( -1.000000000000000000, -0.000000000000000000, -0.000000000000000000 ) ) ;
#29320=ADVANCED_FACE ( 'NONE', ( #14556 ), #36233, .T. ) ;
#29393=SHAPE_REPRESENTATION_RELATIONSHIP ( 'NONE' , 'NONE' ,  #28884, #37568 ) ;
#29410=ADVANCED_FACE ( 'NONE', ( #43614, #2482, #19816 ), #29981, .T. ) ;
#29473=CIRCLE ( 'NONE', #26521, 20.00000000000004619 ) ;
#29534=VERTEX_POINT ( 'NONE', #5264 ) ;
#29566=ORIENTED_EDGE ( 'NONE', *, *, #665, .T. ) ;
#29642=DIRECTION ( 'NONE',  ( 0.000000000000000000, 0.000000000000000000, 1.000000000000000000 ) ) ;
#29682=VECTOR ( 'NONE', #40386, 1000.000000000000000 ) ;
#29843=CLOSED_SHELL ( 'NONE', ( #21418, #35139, #7712, #29410, #22910, #29320, #21031, #26918, #23326, #34902, #24691 ) ) ;
#29876=CIRCLE ( 'NONE', #18855, 19.99999999999990763 ) ;
#29981=PLANE ( 'NONE',  #6986 ) ;
#30404=CIRCLE ( 'NONE', #27467, 10.00000000000000888 ) ;
#30563=ORIENTED_EDGE ( 'NONE', *, *, #12587, .T. ) ;
#30677=DIRECTION ( 'NONE',  ( -1.000000000000000000, -0.000000000000000000, -0.000000000000000000 ) ) ;
#30692=VECTOR ( 'NONE', #4853, 1000.000000000000000 ) ;
#31124=ORIENTED_EDGE ( 'NONE', *, *, #9214, .T. ) ;
#31260=LINE ( 'NONE', #6324, #22825 ) ;
#31339=DIRECTION ( 'NONE',  ( 0.000000000000000000, 0.9235249282889856914, 0.3835384033298670503 ) ) ;
#31471=EDGE_LOOP ( 'NONE', ( #27200, #44763, #31124, #1693 ) ) ;
#31582=VECTOR ( 'NONE', #31339, 1000.000000000000114 ) ;
#31811=VERTEX_POINT ( 'NONE', #27096 ) ;
#31862=VECTOR ( 'NONE', #12134, 1000.000000000000114 ) ;
#31953=PRODUCT_DEFINITION_FORMATION_WITH_SPECIFIED_SOURCE ( 'ANY', '', #2631, .NOT_KNOWN. ) ;
#32001=CYLINDRICAL_SURFACE ( 'NONE', #35943, 20.00000000000004974 ) ;
#32103=LINE ( 'NONE', #28176, #22019 ) ;
#32162=ORIENTED_EDGE ( 'NONE', *, *, #12587, .F. ) ;
#32471=EDGE_LOOP ( 'NONE', ( #36197, #11781 ) ) ;
#32569=EDGE_CURVE ( 'NONE', #40061, #18319, #16681, .T. ) ;
#32586=ORIENTED_EDGE ( 'NONE', *, *, #28336, .F. ) ;
#32621=DIRECTION ( 'NONE',  ( -1.000000000000000000, -0.000000000000000000, 0.000000000000000000 ) ) ;
#32718=LINE ( 'NONE', #8696, #12854 ) ;
#32861=ORIENTED_EDGE ( 'NONE', *, *, #665, .F. ) ;
#32901=PLANE ( 'NONE',  #37276 ) ;
#32937=DIRECTION ( 'NONE',  ( 0.000000000000000000, 0.000000000000000000, -1.000000000000000000 ) ) ;
#33126=DIRECTION ( 'NONE',  ( 1.000000000000000000, 0.000000000000000000, -0.000000000000000000 ) ) ;
#33129=ORIENTED_EDGE ( 'NONE', *, *, #9748, .T. ) ;
#33321=( NAMED_UNIT ( * ) PLANE_ANGLE_UNIT ( ) SI_UNIT ( $, .RADIAN. ) );
#33532=DIRECTION ( 'NONE',  ( -1.000000000000000000, -0.000000000000000000, -0.000000000000000000 ) ) ;
#33822=ORIENTED_EDGE ( 'NONE', *, *, #39112, .F. ) ;
#34241=DIRECTION ( 'NONE',  ( 0.000000000000000000, 0.000000000000000000, 1.000000000000000000 ) ) ;
#34495=EDGE_CURVE ( 'NONE', #31811, #10985, #27094, .T. ) ;
#34902=ADVANCED_FACE ( 'NONE', ( #3984 ), #39573, .F. ) ;
#34936=EDGE_LOOP ( 'NONE', ( #17654, #16772, #15366, #9899 ) ) ;
#34987=MECHANICAL_DESIGN_GEOMETRIC_PRESENTATION_REPRESENTATION('',(#28356),#35718);
#35048=CIRCLE ( 'NONE', #28390, 20.00000000000004619 ) ;
#35118=CIRCLE ( 'NONE', #27738, 10.00000000000000888 ) ;
#35139=ADVANCED_FACE ( 'NONE', ( #43008 ), #4453, .F. ) ;
#35718=( GEOMETRIC_REPRESENTATION_CONTEXT ( 3 ) GLOBAL_UNCERTAINTY_ASSIGNED_CONTEXT ( ( #24248 ) ) GLOBAL_UNIT_ASSIGNED_CONTEXT ( ( #37231, #33321, #19454 ) ) REPRESENTATION_CONTEXT ( 'NONE', 'WORKASPACE' ) );
#35917=EDGE_CURVE ( 'NONE', #29534, #36366, #32103, .T. ) ;
#35943=AXIS2_PLACEMENT_3D ( 'NONE', #372, #606, #32937 ) ;
#36064=DIRECTION ( 'NONE',  ( 0.000000000000000000, 0.000000000000000000, -1.000000000000000000 ) ) ;
#36091=( LENGTH_UNIT ( ) NAMED_UNIT ( * ) SI_UNIT ( .MILLI., .METRE. ) );
#36127=EDGE_CURVE ( 'NONE', #9763, #29534, #3406, .T. ) ;
#36197=ORIENTED_EDGE ( 'NONE', *, *, #23454, .T. ) ;
#36233=CYLINDRICAL_SURFACE ( 'NONE', #39485, 19.99999999999990763 ) ;
#36246=EDGE_LOOP ( 'NONE', ( #3419, #42728 ) ) ;
#36304=DIRECTION ( 'NONE',  ( 0.000000000000000000, 0.000000000000000000, -1.000000000000000000 ) ) ;
#36366=VERTEX_POINT ( 'NONE', #39433 ) ;
#36677=CARTESIAN_POINT ( 'NONE',  ( 799.9999999999993179, -365.3551492539851893, 28.13243251470704109 ) ) ;
#36916=CARTESIAN_POINT ( 'NONE',  ( 794.9999999999993179, 205.0000000000000568, 255.0000000000000000 ) ) ;
#37042=CARTESIAN_POINT ( 'NONE',  ( 799.9999999999993179, 205.0000000000000568, 255.0000000000000000 ) ) ;
#37189=CARTESIAN_POINT ( 'NONE',  ( 799.9999999999993179, 212.6707680665973612, 236.5295014342203785 ) ) ;
#37231=( LENGTH_UNIT ( ) NAMED_UNIT ( * ) SI_UNIT ( .MILLI., .METRE. ) );
#37258=ORIENTED_EDGE ( 'NONE', *, *, #29199, .F. ) ;
#37276=AXIS2_PLACEMENT_3D ( 'NONE', #8406, #33126, #29642 ) ;
#37284=CARTESIAN_POINT ( 'NONE',  ( 794.9999999999993179, -365.3551492539851893, 18.13243251470705886 ) ) ;
#37368=DIRECTION ( 'NONE',  ( 1.000000000000000000, 0.000000000000000000, -0.000000000000000000 ) ) ;
#37568=ADVANCED_BREP_SHAPE_REPRESENTATION ( '', ( #1937, #26858 ), #7608 ) ;
#37960=ORIENTED_EDGE ( 'NONE', *, *, #9748, .F. ) ;
#38180=DIRECTION ( 'NONE',  ( -1.000000000000000000, -0.000000000000000000, 0.000000000000000000 ) ) ;
#38198=VERTEX_POINT ( 'NONE', #6472 ) ;
#38262=DIRECTION ( 'NONE',  ( 0.000000000000000000, 0.3835384033298669948, -0.9235249282889858025 ) ) ;
#38677=VECTOR ( 'NONE', #11767, 1000.000000000000000 ) ;
#38844=EDGE_CURVE ( 'NONE', #5059, #36366, #31260, .T. ) ;
#38877=ORIENTED_EDGE ( 'NONE', *, *, #5233, .F. ) ;
#39112=EDGE_CURVE ( 'NONE', #40969, #5059, #29473, .T. ) ;
#39174=EDGE_LOOP ( 'NONE', ( #33129, #15463 ) ) ;
#39181=LINE ( 'NONE', #43313, #41734 ) ;
#39328=ORIENTED_EDGE ( 'NONE', *, *, #28880, .T. ) ;
#39433=CARTESIAN_POINT ( 'NONE',  ( 794.9999999999993179, 197.3292319334027241, 273.4704985657796783 ) ) ;
#39485=AXIS2_PLACEMENT_3D ( 'NONE', #11076, #18689, #1125 ) ;
#39573=CYLINDRICAL_SURFACE ( 'NONE', #3530, 9.999999999999980460 ) ;
#39863=VERTEX_POINT ( 'NONE', #12519 ) ;
#40061=VERTEX_POINT ( 'NONE', #3257 ) ;
#40360=CIRCLE ( 'NONE', #20415, 10.00000000000000888 ) ;
#40386=DIRECTION ( 'NONE',  ( -1.000000000000000000, -0.000000000000000000, 0.000000000000000000 ) ) ;
#40416=ORIENTED_EDGE ( 'NONE', *, *, #35917, .F. ) ;
#40427=FACE_OUTER_BOUND ( 'NONE', #31471, .T. ) ;
#40463=DIRECTION ( 'NONE',  ( 0.000000000000000000, 0.000000000000000000, -1.000000000000000000 ) ) ;
#40515=CARTESIAN_POINT ( 'NONE',  ( 799.9999999999993179, -365.3551492539851893, 18.13243251470705886 ) ) ;
#40598=DIRECTION ( 'NONE',  ( 0.000000000000000000, 0.000000000000000000, 1.000000000000000000 ) ) ;
#40613=CARTESIAN_POINT ( 'NONE',  ( 799.9999999999993179, 205.0000000000000568, 255.0000000000000000 ) ) ;
#40639=DIRECTION ( 'NONE',  ( -1.000000000000000000, -0.000000000000000000, 0.000000000000000000 ) ) ;
#40665=LINE ( 'NONE', #37189, #19555 ) ;
#40690=CARTESIAN_POINT ( 'NONE',  ( 799.9999999999993179, 205.0000000000000568, 255.0000000000000000 ) ) ;
#40876=VECTOR ( 'NONE', #19156, 1000.000000000000000 ) ;
#40907=PRODUCT_CONTEXT ( 'NONE', #10433, 'mechanical' ) ;
#40917=ORIENTED_EDGE ( 'NONE', *, *, #41837, .T. ) ;
#40969=VERTEX_POINT ( 'NONE', #20066 ) ;
#41102=DIRECTION ( 'NONE',  ( 0.000000000000000000, 0.000000000000000000, -1.000000000000000000 ) ) ;
#41291=CARTESIAN_POINT ( 'NONE',  ( 799.9999999999993179, 197.3292319334027241, 273.4704985657796783 ) ) ;
#41427=ORIENTED_EDGE ( 'NONE', *, *, #41642, .T. ) ;
#41642=EDGE_CURVE ( 'NONE', #10343, #22935, #11522, .T. ) ;
#41706=EDGE_LOOP ( 'NONE', ( #24490, #22050, #17418, #42120 ) ) ;
#41727=FACE_OUTER_BOUND ( 'NONE', #41706, .T. ) ;
#41734=VECTOR ( 'NONE', #11000, 1000.000000000000000 ) ;
#41754=AXIS2_PLACEMENT_3D ( 'NONE', #9863, #23935, #45203 ) ;
#41779=AXIS2_PLACEMENT_3D ( 'NONE', #27005, #40639, #41102 ) ;
#41837=EDGE_CURVE ( 'NONE', #18319, #40061, #30404, .T. ) ;
#41957=DIRECTION ( 'NONE',  ( -1.000000000000000000, -0.000000000000000000, -0.000000000000000000 ) ) ;
#42120=ORIENTED_EDGE ( 'NONE', *, *, #35917, .T. ) ;
#42171=CARTESIAN_POINT ( 'NONE',  ( 799.9999999999993179, 205.0000000000000568, 245.0000000000000284 ) ) ;
#42200=ORIENTED_EDGE ( 'NONE', *, *, #20424, .T. ) ;
#42437=ORIENTED_EDGE ( 'NONE', *, *, #3789, .T. ) ;
#42700=VERTEX_POINT ( 'NONE', #24387 ) ;
#42728=ORIENTED_EDGE ( 'NONE', *, *, #41837, .F. ) ;
#42912=ORIENTED_EDGE ( 'NONE', *, *, #19596, .F. ) ;
#42921=EDGE_LOOP ( 'NONE', ( #26467, #3931, #30563, #22983 ) ) ;
#42935=CARTESIAN_POINT ( 'NONE',  ( 799.9999999999993179, -365.3551492539851893, -1.867567485292990437 ) ) ;
#43008=FACE_OUTER_BOUND ( 'NONE', #20560, .T. ) ;
#43156=DIRECTION ( 'NONE',  ( -1.000000000000000000, -0.000000000000000000, -0.000000000000000000 ) ) ;
#43313=CARTESIAN_POINT ( 'NONE',  ( 799.9999999999993179, -365.3551492539851893, 8.132432514707076621 ) ) ;
#43464=ORIENTED_EDGE ( 'NONE', *, *, #9214, .F. ) ;
#43566=EDGE_LOOP ( 'NONE', ( #44299, #19484, #28659, #45536, #8199 ) ) ;
#43614=FACE_BOUND ( 'NONE', #39174, .T. ) ;
#43645=CARTESIAN_POINT ( 'NONE',  ( 799.9999999999993179, -373.0259173205825505, 36.60293108048681887 ) ) ;
#43857=EDGE_LOOP ( 'NONE', ( #14702, #28768, #32861, #18238, #32162 ) ) ;
#43961=PRODUCT_DEFINITION_CONTEXT ( 'detailed design', #15185, 'design' ) ;
#44217=DIRECTION ( 'NONE',  ( -1.000000000000000000, -0.000000000000000000, -0.000000000000000000 ) ) ;
#44299=ORIENTED_EDGE ( 'NONE', *, *, #4000, .T. ) ;
#44616=CARTESIAN_POINT ( 'NONE',  ( 799.9999999999993179, -365.3551492539851893, -1.867567485292990437 ) ) ;
#44763=ORIENTED_EDGE ( 'NONE', *, *, #23454, .F. ) ;
#44896=VERTEX_POINT ( 'NONE', #11700 ) ;
#45100=CARTESIAN_POINT ( 'NONE',  ( 799.9999999999993179, -365.3551492539851893, 18.13243251470705886 ) ) ;
#45203=DIRECTION ( 'NONE',  ( 0.000000000000000000, 0.000000000000000000, 1.000000000000000000 ) ) ;
#45362=DIRECTION ( 'NONE',  ( -1.000000000000000000, -0.000000000000000000, -0.000000000000000000 ) ) ;
#45464=VECTOR ( 'NONE', #15383, 1000.000000000000114 ) ;
#45520=UNCERTAINTY_MEASURE_WITH_UNIT (LENGTH_MEASURE( 1.000000000000000082E-05 ), #36091, 'distance_accuracy_value', 'NONE');
#45536=ORIENTED_EDGE ( 'NONE', *, *, #39112, .T. ) ;
#45745=COLOUR_RGB('Light Blue',0.38,0.62,0.78);
#45746=FILL_AREA_STYLE_COLOUR('',#45745);
#45747=FILL_AREA_STYLE('',(#45746));
#45748=SURFACE_STYLE_FILL_AREA(#45747);
#45749=SURFACE_SIDE_STYLE('',(#45748));
#45750=SURFACE_STYLE_USAGE(.BOTH.,#45749);
#45751=PRESENTATION_STYLE_ASSIGNMENT((#45750));
ENDSEC;
END-ISO-10303-21;
